ISO-10303-21;
HEADER;
/* Generated by software containing ST-Developer
 * from STEP Tools, Inc. (www.steptools.com) 
 */

FILE_DESCRIPTION(
/* description */ ('Over-Centre Plunger Toggle Clamp on Slotted Fixture Frame'),
/* implementation_level */ '2;1');

FILE_NAME(
/* name */ 
'Socket Set Screw - M4x6.step',
/* time_stamp */ '2026-10-28T03:23:24-07:00',
/* author */ (''),
/* organization */ (''),
/* preprocessor_version */ 'ST-DEVELOPER v20.2',
/* originating_system */ 'Autodesk Translation Framework v15.17.0.0',
/* authorisation */ '');

FILE_SCHEMA (('AUTOMOTIVE_DESIGN { 1 0 10303 214 3 1 1 }'));
ENDSEC;

DATA;
#10=MECHANICAL_DESIGN_GEOMETRIC_PRESENTATION_REPRESENTATION('',(#563),#15212);
#425=CONICAL_SURFACE('',#9739,0.185,0.785398163397449);
#426=CONICAL_SURFACE('',#9743,0.1625,0.785398163397449);
#470=SHAPE_REPRESENTATION_RELATIONSHIP('SRR','None',#15449,#512);
#512=ADVANCED_BREP_SHAPE_REPRESENTATION('',(#610),#15211);
#563=STYLED_ITEM('',(#15726),#610);
#610=MANIFOLD_SOLID_BREP('Body1',#8299);
#782=FACE_BOUND('',#2226,.T.);
#1078=PLANE('',#9730);
#1079=PLANE('',#9731);
#1080=PLANE('',#9732);
#1081=PLANE('',#9733);
#1082=PLANE('',#9734);
#1083=PLANE('',#9735);
#1084=PLANE('',#9736);
#1085=PLANE('',#9737);
#1086=PLANE('',#9745);
#1561=FACE_OUTER_BOUND('',#2218,.T.);
#1562=FACE_OUTER_BOUND('',#2219,.T.);
#1563=FACE_OUTER_BOUND('',#2220,.T.);
#1564=FACE_OUTER_BOUND('',#2221,.T.);
#1565=FACE_OUTER_BOUND('',#2222,.T.);
#1566=FACE_OUTER_BOUND('',#2223,.T.);
#1567=FACE_OUTER_BOUND('',#2224,.T.);
#1568=FACE_OUTER_BOUND('',#2225,.T.);
#1569=FACE_OUTER_BOUND('',#2227,.T.);
#1570=FACE_OUTER_BOUND('',#2228,.T.);
#1571=FACE_OUTER_BOUND('',#2229,.T.);
#1572=FACE_OUTER_BOUND('',#2230,.T.);
#2218=EDGE_LOOP('',(#7567,#7568,#7569,#7570));
#2219=EDGE_LOOP('',(#7571,#7572,#7573,#7574));
#2220=EDGE_LOOP('',(#7575,#7576,#7577,#7578));
#2221=EDGE_LOOP('',(#7579,#7580,#7581,#7582));
#2222=EDGE_LOOP('',(#7583,#7584,#7585,#7586));
#2223=EDGE_LOOP('',(#7587,#7588,#7589,#7590));
#2224=EDGE_LOOP('',(#7591,#7592,#7593,#7594,#7595,#7596));
#2225=EDGE_LOOP('',(#7597));
#2226=EDGE_LOOP('',(#7598,#7599,#7600,#7601,#7602,#7603));
#2227=EDGE_LOOP('',(#7604,#7605,#7606,#7607));
#2228=EDGE_LOOP('',(#7608,#7609,#7610,#7611));
#2229=EDGE_LOOP('',(#7612,#7613,#7614,#7615));
#2230=EDGE_LOOP('',(#7616));
#2840=LINE('',#15055,#3470);
#2841=LINE('',#15057,#3471);
#2842=LINE('',#15059,#3472);
#2843=LINE('',#15060,#3473);
#2844=LINE('',#15063,#3474);
#2845=LINE('',#15065,#3475);
#2846=LINE('',#15066,#3476);
#2847=LINE('',#15069,#3477);
#2848=LINE('',#15071,#3478);
#2849=LINE('',#15072,#3479);
#2850=LINE('',#15075,#3480);
#2851=LINE('',#15077,#3481);
#2852=LINE('',#15078,#3482);
#2853=LINE('',#15081,#3483);
#2854=LINE('',#15083,#3484);
#2855=LINE('',#15084,#3485);
#2856=LINE('',#15086,#3486);
#2857=LINE('',#15087,#3487);
#2858=LINE('',#15095,#3488);
#2859=LINE('',#15099,#3489);
#2860=LINE('',#15103,#3490);
#3470=VECTOR('',#12299,1.);
#3471=VECTOR('',#12300,1.);
#3472=VECTOR('',#12301,1.);
#3473=VECTOR('',#12302,1.);
#3474=VECTOR('',#12305,1.);
#3475=VECTOR('',#12306,1.);
#3476=VECTOR('',#12307,1.);
#3477=VECTOR('',#12310,1.);
#3478=VECTOR('',#12311,1.);
#3479=VECTOR('',#12312,1.);
#3480=VECTOR('',#12315,1.);
#3481=VECTOR('',#12316,1.);
#3482=VECTOR('',#12317,1.);
#3483=VECTOR('',#12320,1.);
#3484=VECTOR('',#12321,1.);
#3485=VECTOR('',#12322,1.);
#3486=VECTOR('',#12325,1.);
#3487=VECTOR('',#12326,1.);
#3488=VECTOR('',#12337,0.185);
#3489=VECTOR('',#12342,0.2);
#3490=VECTOR('',#12347,0.1625);
#3855=CIRCLE('',#9738,0.17);
#3856=CIRCLE('',#9740,0.1954);
#3857=CIRCLE('',#9742,0.1954);
#3858=CIRCLE('',#9744,0.125);
#4529=VERTEX_POINT('',#15053);
#4530=VERTEX_POINT('',#15054);
#4531=VERTEX_POINT('',#15056);
#4532=VERTEX_POINT('',#15058);
#4533=VERTEX_POINT('',#15062);
#4534=VERTEX_POINT('',#15064);
#4535=VERTEX_POINT('',#15068);
#4536=VERTEX_POINT('',#15070);
#4537=VERTEX_POINT('',#15074);
#4538=VERTEX_POINT('',#15076);
#4539=VERTEX_POINT('',#15080);
#4540=VERTEX_POINT('',#15082);
#4541=VERTEX_POINT('',#15090);
#4542=VERTEX_POINT('',#15093);
#4543=VERTEX_POINT('',#15097);
#4544=VERTEX_POINT('',#15101);
#5544=EDGE_CURVE('',#4529,#4530,#2840,.T.);
#5545=EDGE_CURVE('',#4529,#4531,#2841,.T.);
#5546=EDGE_CURVE('',#4531,#4532,#2842,.T.);
#5547=EDGE_CURVE('',#4530,#4532,#2843,.T.);
#5548=EDGE_CURVE('',#4533,#4529,#2844,.T.);
#5549=EDGE_CURVE('',#4533,#4534,#2845,.T.);
#5550=EDGE_CURVE('',#4534,#4531,#2846,.T.);
#5551=EDGE_CURVE('',#4535,#4533,#2847,.T.);
#5552=EDGE_CURVE('',#4535,#4536,#2848,.T.);
#5553=EDGE_CURVE('',#4536,#4534,#2849,.T.);
#5554=EDGE_CURVE('',#4537,#4535,#2850,.T.);
#5555=EDGE_CURVE('',#4537,#4538,#2851,.T.);
#5556=EDGE_CURVE('',#4538,#4536,#2852,.T.);
#5557=EDGE_CURVE('',#4539,#4537,#2853,.T.);
#5558=EDGE_CURVE('',#4539,#4540,#2854,.T.);
#5559=EDGE_CURVE('',#4540,#4538,#2855,.T.);
#5560=EDGE_CURVE('',#4530,#4539,#2856,.T.);
#5561=EDGE_CURVE('',#4532,#4540,#2857,.T.);
#5562=EDGE_CURVE('',#4541,#4541,#3855,.T.);
#5563=EDGE_CURVE('',#4542,#4542,#3856,.T.);
#5564=EDGE_CURVE('',#4542,#4541,#2858,.T.);
#5565=EDGE_CURVE('',#4543,#4543,#3857,.F.);
#5566=EDGE_CURVE('',#4543,#4542,#2859,.T.);
#5567=EDGE_CURVE('',#4544,#4544,#3858,.T.);
#5568=EDGE_CURVE('',#4544,#4543,#2860,.T.);
#7567=ORIENTED_EDGE('',*,*,#5544,.F.);
#7568=ORIENTED_EDGE('',*,*,#5545,.T.);
#7569=ORIENTED_EDGE('',*,*,#5546,.T.);
#7570=ORIENTED_EDGE('',*,*,#5547,.F.);
#7571=ORIENTED_EDGE('',*,*,#5548,.F.);
#7572=ORIENTED_EDGE('',*,*,#5549,.T.);
#7573=ORIENTED_EDGE('',*,*,#5550,.T.);
#7574=ORIENTED_EDGE('',*,*,#5545,.F.);
#7575=ORIENTED_EDGE('',*,*,#5551,.F.);
#7576=ORIENTED_EDGE('',*,*,#5552,.T.);
#7577=ORIENTED_EDGE('',*,*,#5553,.T.);
#7578=ORIENTED_EDGE('',*,*,#5549,.F.);
#7579=ORIENTED_EDGE('',*,*,#5554,.F.);
#7580=ORIENTED_EDGE('',*,*,#5555,.T.);
#7581=ORIENTED_EDGE('',*,*,#5556,.T.);
#7582=ORIENTED_EDGE('',*,*,#5552,.F.);
#7583=ORIENTED_EDGE('',*,*,#5557,.F.);
#7584=ORIENTED_EDGE('',*,*,#5558,.T.);
#7585=ORIENTED_EDGE('',*,*,#5559,.T.);
#7586=ORIENTED_EDGE('',*,*,#5555,.F.);
#7587=ORIENTED_EDGE('',*,*,#5560,.F.);
#7588=ORIENTED_EDGE('',*,*,#5547,.T.);
#7589=ORIENTED_EDGE('',*,*,#5561,.T.);
#7590=ORIENTED_EDGE('',*,*,#5558,.F.);
#7591=ORIENTED_EDGE('',*,*,#5561,.F.);
#7592=ORIENTED_EDGE('',*,*,#5546,.F.);
#7593=ORIENTED_EDGE('',*,*,#5550,.F.);
#7594=ORIENTED_EDGE('',*,*,#5553,.F.);
#7595=ORIENTED_EDGE('',*,*,#5556,.F.);
#7596=ORIENTED_EDGE('',*,*,#5559,.F.);
#7597=ORIENTED_EDGE('',*,*,#5562,.F.);
#7598=ORIENTED_EDGE('',*,*,#5544,.T.);
#7599=ORIENTED_EDGE('',*,*,#5560,.T.);
#7600=ORIENTED_EDGE('',*,*,#5557,.T.);
#7601=ORIENTED_EDGE('',*,*,#5554,.T.);
#7602=ORIENTED_EDGE('',*,*,#5551,.T.);
#7603=ORIENTED_EDGE('',*,*,#5548,.T.);
#7604=ORIENTED_EDGE('',*,*,#5563,.F.);
#7605=ORIENTED_EDGE('',*,*,#5564,.T.);
#7606=ORIENTED_EDGE('',*,*,#5562,.T.);
#7607=ORIENTED_EDGE('',*,*,#5564,.F.);
#7608=ORIENTED_EDGE('',*,*,#5565,.F.);
#7609=ORIENTED_EDGE('',*,*,#5566,.T.);
#7610=ORIENTED_EDGE('',*,*,#5563,.T.);
#7611=ORIENTED_EDGE('',*,*,#5566,.F.);
#7612=ORIENTED_EDGE('',*,*,#5567,.F.);
#7613=ORIENTED_EDGE('',*,*,#5568,.T.);
#7614=ORIENTED_EDGE('',*,*,#5565,.T.);
#7615=ORIENTED_EDGE('',*,*,#5568,.F.);
#7616=ORIENTED_EDGE('',*,*,#5567,.T.);
#7758=CYLINDRICAL_SURFACE('',#9741,0.1954);
#8233=ADVANCED_FACE('',(#1561),#1078,.F.);
#8234=ADVANCED_FACE('',(#1562),#1079,.F.);
#8235=ADVANCED_FACE('',(#1563),#1080,.F.);
#8236=ADVANCED_FACE('',(#1564),#1081,.F.);
#8237=ADVANCED_FACE('',(#1565),#1082,.F.);
#8238=ADVANCED_FACE('',(#1566),#1083,.F.);
#8239=ADVANCED_FACE('',(#1567),#1084,.F.);
#8240=ADVANCED_FACE('',(#1568,#782),#1085,.T.);
#8241=ADVANCED_FACE('',(#1569),#425,.T.);
#8242=ADVANCED_FACE('',(#1570),#7758,.T.);
#8243=ADVANCED_FACE('',(#1571),#426,.T.);
#8244=ADVANCED_FACE('',(#1572),#1086,.T.);
#8299=CLOSED_SHELL('',(#8233,#8234,#8235,#8236,#8237,#8238,#8239,#8240,
#8241,#8242,#8243,#8244));
#9729=AXIS2_PLACEMENT_3D('',#15051,#12295,#12296);
#9730=AXIS2_PLACEMENT_3D('',#15052,#12297,#12298);
#9731=AXIS2_PLACEMENT_3D('',#15061,#12303,#12304);
#9732=AXIS2_PLACEMENT_3D('',#15067,#12308,#12309);
#9733=AXIS2_PLACEMENT_3D('',#15073,#12313,#12314);
#9734=AXIS2_PLACEMENT_3D('',#15079,#12318,#12319);
#9735=AXIS2_PLACEMENT_3D('',#15085,#12323,#12324);
#9736=AXIS2_PLACEMENT_3D('',#15088,#12327,#12328);
#9737=AXIS2_PLACEMENT_3D('',#15089,#12329,#12330);
#9738=AXIS2_PLACEMENT_3D('',#15091,#12331,#12332);
#9739=AXIS2_PLACEMENT_3D('',#15092,#12333,#12334);
#9740=AXIS2_PLACEMENT_3D('',#15094,#12335,#12336);
#9741=AXIS2_PLACEMENT_3D('',#15096,#12338,#12339);
#9742=AXIS2_PLACEMENT_3D('',#15098,#12340,#12341);
#9743=AXIS2_PLACEMENT_3D('',#15100,#12343,#12344);
#9744=AXIS2_PLACEMENT_3D('',#15102,#12345,#12346);
#9745=AXIS2_PLACEMENT_3D('',#15104,#12348,#12349);
#12295=DIRECTION('axis',(0.,0.,1.));
#12296=DIRECTION('refdir',(1.,0.,0.));
#12297=DIRECTION('center_axis',(0.866025403784439,0.,-0.5));
#12298=DIRECTION('ref_axis',(0.5,0.,0.866025403784439));
#12299=DIRECTION('',(0.5,0.,0.866025403784439));
#12300=DIRECTION('',(0.,-1.,0.));
#12301=DIRECTION('',(0.5,0.,0.866025403784439));
#12302=DIRECTION('',(0.,-1.,0.));
#12303=DIRECTION('center_axis',(1.20185167898973E-16,0.,-1.));
#12304=DIRECTION('ref_axis',(1.,0.,1.20185167898973E-16));
#12305=DIRECTION('',(1.,0.,1.20185167898973E-16));
#12306=DIRECTION('',(0.,-1.,0.));
#12307=DIRECTION('',(1.,0.,1.20185167898973E-16));
#12308=DIRECTION('center_axis',(-0.866025403784439,0.,-0.5));
#12309=DIRECTION('ref_axis',(0.5,0.,-0.866025403784439));
#12310=DIRECTION('',(0.5,0.,-0.866025403784439));
#12311=DIRECTION('',(0.,-1.,0.));
#12312=DIRECTION('',(0.5,0.,-0.866025403784439));
#12313=DIRECTION('center_axis',(-0.866025403784439,0.,0.5));
#12314=DIRECTION('ref_axis',(-0.5,0.,-0.866025403784439));
#12315=DIRECTION('',(-0.5,0.,-0.866025403784439));
#12316=DIRECTION('',(0.,-1.,0.));
#12317=DIRECTION('',(-0.5,0.,-0.866025403784439));
#12318=DIRECTION('center_axis',(-2.40370335797945E-16,0.,1.));
#12319=DIRECTION('ref_axis',(-1.,0.,-2.40370335797945E-16));
#12320=DIRECTION('',(-1.,0.,-2.40370335797945E-16));
#12321=DIRECTION('',(0.,-1.,0.));
#12322=DIRECTION('',(-1.,0.,-2.40370335797945E-16));
#12323=DIRECTION('center_axis',(0.866025403784439,0.,0.5));
#12324=DIRECTION('ref_axis',(-0.5,0.,0.866025403784439));
#12325=DIRECTION('',(-0.5,0.,0.866025403784439));
#12326=DIRECTION('',(-0.5,0.,0.866025403784439));
#12327=DIRECTION('center_axis',(0.,-1.,0.));
#12328=DIRECTION('ref_axis',(0.,0.,-1.));
#12329=DIRECTION('center_axis',(0.,1.,0.));
#12330=DIRECTION('ref_axis',(0.,0.,1.));
#12331=DIRECTION('center_axis',(0.,-1.,0.));
#12332=DIRECTION('ref_axis',(1.,0.,0.));
#12333=DIRECTION('center_axis',(0.,-1.,0.));
#12334=DIRECTION('ref_axis',(1.,0.,0.));
#12335=DIRECTION('center_axis',(0.,-1.,0.));
#12336=DIRECTION('ref_axis',(1.,0.,0.));
#12337=DIRECTION('',(0.707106781186548,0.707106781186547,8.65956056235494E-17));
#12338=DIRECTION('center_axis',(0.,-1.,0.));
#12339=DIRECTION('ref_axis',(1.,0.,0.));
#12340=DIRECTION('center_axis',(0.,1.,0.));
#12341=DIRECTION('ref_axis',(1.,0.,0.));
#12342=DIRECTION('',(0.,1.,0.));
#12343=DIRECTION('center_axis',(0.,1.,0.));
#12344=DIRECTION('ref_axis',(1.,0.,0.));
#12345=DIRECTION('center_axis',(0.,-1.,0.));
#12346=DIRECTION('ref_axis',(1.,0.,0.));
#12347=DIRECTION('',(-0.707106781186548,0.707106781186547,-8.65956056235494E-17));
#12348=DIRECTION('center_axis',(0.,-1.,0.));
#12349=DIRECTION('ref_axis',(0.,0.,-1.));
#15051=CARTESIAN_POINT('',(0.,0.,0.));
#15052=CARTESIAN_POINT('Origin',(0.0577350269189626,0.,-0.1));
#15053=CARTESIAN_POINT('',(0.0577350269189626,0.,-0.1));
#15054=CARTESIAN_POINT('',(0.115470053837925,0.,0.));
#15055=CARTESIAN_POINT('',(0.0934187836487032,0.,-0.0381939203391614));
#15056=CARTESIAN_POINT('',(0.0577350269189626,-0.2,-0.1));
#15057=CARTESIAN_POINT('',(0.0577350269189626,0.,-0.1));
#15058=CARTESIAN_POINT('',(0.115470053837925,-0.2,0.));
#15059=CARTESIAN_POINT('',(0.115470053837925,-0.2,0.));
#15060=CARTESIAN_POINT('',(0.115470053837925,0.,0.));
#15061=CARTESIAN_POINT('Origin',(-0.0577350269189626,0.,-0.1));
#15062=CARTESIAN_POINT('',(-0.0577350269189626,0.,-0.1));
#15063=CARTESIAN_POINT('',(0.0561324865405187,0.,-0.1));
#15064=CARTESIAN_POINT('',(-0.0577350269189626,-0.2,-0.1));
#15065=CARTESIAN_POINT('',(-0.0577350269189626,0.,-0.1));
#15066=CARTESIAN_POINT('',(0.0577350269189626,-0.2,-0.1));
#15067=CARTESIAN_POINT('Origin',(-0.115470053837925,0.,-1.38777878078145E-17));
#15068=CARTESIAN_POINT('',(-0.115470053837925,0.,-1.41410031829988E-17));
#15069=CARTESIAN_POINT('',(-0.0797862971081845,0.,-0.0618060796608387));
#15070=CARTESIAN_POINT('',(-0.115470053837925,-0.2,-1.38777878078145E-17));
#15071=CARTESIAN_POINT('',(-0.115470053837925,0.,-1.41410031829988E-17));
#15072=CARTESIAN_POINT('',(-0.0577350269189626,-0.2,-0.1));
#15073=CARTESIAN_POINT('Origin',(-0.0577350269189626,0.,0.1));
#15074=CARTESIAN_POINT('',(-0.0577350269189626,0.,0.1));
#15075=CARTESIAN_POINT('',(-0.0509187836487033,0.,0.111806079660839));
#15076=CARTESIAN_POINT('',(-0.0577350269189626,-0.2,0.1));
#15077=CARTESIAN_POINT('',(-0.0577350269189626,0.,0.1));
#15078=CARTESIAN_POINT('',(-0.115470053837925,-0.2,-1.41410031829988E-17));
#15079=CARTESIAN_POINT('Origin',(0.0577350269189626,0.,0.1));
#15080=CARTESIAN_POINT('',(0.0577350269189626,0.,0.1));
#15081=CARTESIAN_POINT('',(0.113867513459481,0.,0.1));
#15082=CARTESIAN_POINT('',(0.0577350269189626,-0.2,0.1));
#15083=CARTESIAN_POINT('',(0.0577350269189626,0.,0.1));
#15084=CARTESIAN_POINT('',(-0.0577350269189626,-0.2,0.1));
#15085=CARTESIAN_POINT('Origin',(0.115470053837925,0.,0.));
#15086=CARTESIAN_POINT('',(0.122286297108185,0.,-0.0118060796608386));
#15087=CARTESIAN_POINT('',(0.0577350269189626,-0.2,0.1));
#15088=CARTESIAN_POINT('Origin',(0.,-0.2,0.));
#15089=CARTESIAN_POINT('Origin',(0.17,0.,0.));
#15090=CARTESIAN_POINT('',(-0.17,-8.67361737988404E-18,-2.0818995585505E-17));
#15091=CARTESIAN_POINT('Origin',(0.,0.,0.));
#15092=CARTESIAN_POINT('Origin',(0.,-0.015,0.));
#15093=CARTESIAN_POINT('',(-0.1954,-0.0254,-2.39295984553393E-17));
#15094=CARTESIAN_POINT('Origin',(0.,-0.0254,0.));
#15095=CARTESIAN_POINT('',(-0.185,-0.015,-2.2655965784226E-17));
#15096=CARTESIAN_POINT('Origin',(0.,-0.2775,0.));
#15097=CARTESIAN_POINT('',(-0.1954,-0.5296,2.39295984553393E-17));
#15098=CARTESIAN_POINT('Origin',(0.,-0.5296,0.));
#15099=CARTESIAN_POINT('',(-0.1954,-0.2775,-2.39295984553393E-17));
#15100=CARTESIAN_POINT('Origin',(0.,-0.5625,0.));
#15101=CARTESIAN_POINT('',(-0.125,-0.6,-1.53080849893419E-17));
#15102=CARTESIAN_POINT('Origin',(0.,-0.6,0.));
#15103=CARTESIAN_POINT('',(-0.1625,-0.5625,-1.99005104861445E-17));
#15104=CARTESIAN_POINT('Origin',(0.,-0.6,0.));
#15161=UNCERTAINTY_MEASURE_WITH_UNIT(LENGTH_MEASURE(0.001),#15213,
'DISTANCE_ACCURACY_VALUE',
'Maximum model space distance between geometric entities at asserted c
onnectivities');
#15162=UNCERTAINTY_MEASURE_WITH_UNIT(LENGTH_MEASURE(0.001),#15213,
'DISTANCE_ACCURACY_VALUE',
'Maximum model space distance between geometric entities at asserted c
onnectivities');
#15211=(
GEOMETRIC_REPRESENTATION_CONTEXT(3)
GLOBAL_UNCERTAINTY_ASSIGNED_CONTEXT((#15161))
GLOBAL_UNIT_ASSIGNED_CONTEXT((#15213,#15215,#15216))
REPRESENTATION_CONTEXT('','3D')
);
#15212=(
GEOMETRIC_REPRESENTATION_CONTEXT(3)
GLOBAL_UNCERTAINTY_ASSIGNED_CONTEXT((#15162))
GLOBAL_UNIT_ASSIGNED_CONTEXT((#15213,#15215,#15216))
REPRESENTATION_CONTEXT('','3D')
);
#15213=(
LENGTH_UNIT()
NAMED_UNIT(*)
SI_UNIT(.CENTI.,.METRE.)
);
#15215=(
NAMED_UNIT(*)
PLANE_ANGLE_UNIT()
SI_UNIT($,.RADIAN.)
);
#15216=(
NAMED_UNIT(*)
SI_UNIT($,.STERADIAN.)
SOLID_ANGLE_UNIT()
);
#15265=SHAPE_DEFINITION_REPRESENTATION(#15392,#15449);
#15392=PRODUCT_DEFINITION_SHAPE('',$,#15499);
#15449=SHAPE_REPRESENTATION('',(#9729),#15211);
#15450=PRODUCT_DEFINITION_CONTEXT('part definition',#15599,'design');
#15499=PRODUCT_DEFINITION('Socket Set Screw - M4x6',
'Socket Set Screw - M4x6',#15548,#15450);
#15548=PRODUCT_DEFINITION_FORMATION('',$,#15649);
#15599=APPLICATION_CONTEXT(
'Core Data for Automotive Mechanical Design Process');
#15600=PRODUCT_CONTEXT('part definition',#15599,'mechanical');
#15649=PRODUCT('Socket Set Screw - M4x6','Socket Set Screw - M4x6',
'Socket Set Screw - M4x6',(#15600));
#15720=COLOUR_RGB('Black',0.12,0.14,0.17);
#15721=FILL_AREA_STYLE_COLOUR('',#15720);
#15722=FILL_AREA_STYLE('',(#15721));
#15723=SURFACE_STYLE_FILL_AREA(#15722);
#15724=SURFACE_SIDE_STYLE('',(#15723));
#15725=SURFACE_STYLE_USAGE(.BOTH.,#15724);
#15726=PRESENTATION_STYLE_ASSIGNMENT((#15725));
ENDSEC;
END-ISO-10303-21;
